ISO-10303-21;
HEADER;
/* Generated by software containing ST-Developer
 * from STEP Tools, Inc. (www.steptools.com) 
 */

FILE_DESCRIPTION(
/* description */ ('STEP AP214'),
/* implementation_level */ '2;1');

FILE_NAME(
/* name */ 'Low Head Cap Screw M8x45.step',
/* time_stamp */ '2026-11-15T14:55:55-08:00',
/* author */ (''),
/* organization */ (''),
/* preprocessor_version */ 'ST-DEVELOPER v20.2',
/* originating_system */ 'Autodesk Translation Framework v15.17.0.0',
/* authorisation */ '');

FILE_SCHEMA (('AUTOMOTIVE_DESIGN { 1 0 10303 214 3 1 1 }'));
ENDSEC;

DATA;
#10=MECHANICAL_DESIGN_GEOMETRIC_PRESENTATION_REPRESENTATION('',(#958,#959,#960),#57079);
#894=SHAPE_REPRESENTATION_RELATIONSHIP('SRR','None',#57284,#923);
#923=ADVANCED_BREP_SHAPE_REPRESENTATION('',(#995,#996,#997),#57076);
#958=STYLED_ITEM('',(#57444),#995);
#959=STYLED_ITEM('',(#57444),#996);
#960=STYLED_ITEM('',(#57444),#997);
#995=MANIFOLD_SOLID_BREP('Body1',#24558);
#996=MANIFOLD_SOLID_BREP('Body2',#24559);
#997=MANIFOLD_SOLID_BREP('Body3',#24560);
#1333=FACE_BOUND('',#5189,.T.);
#1334=FACE_BOUND('',#5192,.T.);
#1335=FACE_BOUND('',#5194,.T.);
#1336=FACE_BOUND('',#5210,.T.);
#1337=FACE_BOUND('',#5212,.T.);
#2063=PLANE('',#27336);
#2064=PLANE('',#27337);
#2065=PLANE('',#27338);
#2066=PLANE('',#27339);
#2067=PLANE('',#27340);
#2068=PLANE('',#27341);
#2069=PLANE('',#27342);
#2070=PLANE('',#27343);
#2071=PLANE('',#27344);
#2072=PLANE('',#27345);
#2073=PLANE('',#27346);
#2074=PLANE('',#27347);
#2075=PLANE('',#27348);
#2076=PLANE('',#27349);
#2077=PLANE('',#27350);
#2078=PLANE('',#27351);
#2079=PLANE('',#27358);
#2080=PLANE('',#27359);
#2081=PLANE('',#27366);
#2082=PLANE('',#27367);
#2083=PLANE('',#27368);
#2084=PLANE('',#27369);
#2153=CONICAL_SURFACE('',#27316,5.7,0.785398163397444);
#2154=CONICAL_SURFACE('',#27320,1664.2794823505,1.02974425867665);
#3475=FACE_OUTER_BOUND('',#5183,.T.);
#3476=FACE_OUTER_BOUND('',#5184,.T.);
#3477=FACE_OUTER_BOUND('',#5185,.T.);
#3478=FACE_OUTER_BOUND('',#5186,.T.);
#3479=FACE_OUTER_BOUND('',#5187,.T.);
#3480=FACE_OUTER_BOUND('',#5188,.T.);
#3481=FACE_OUTER_BOUND('',#5190,.T.);
#3482=FACE_OUTER_BOUND('',#5191,.T.);
#3483=FACE_OUTER_BOUND('',#5193,.T.);
#3484=FACE_OUTER_BOUND('',#5195,.T.);
#3485=FACE_OUTER_BOUND('',#5196,.T.);
#3486=FACE_OUTER_BOUND('',#5197,.T.);
#3487=FACE_OUTER_BOUND('',#5198,.T.);
#3488=FACE_OUTER_BOUND('',#5199,.T.);
#3489=FACE_OUTER_BOUND('',#5200,.T.);
#3490=FACE_OUTER_BOUND('',#5201,.T.);
#3491=FACE_OUTER_BOUND('',#5202,.T.);
#3492=FACE_OUTER_BOUND('',#5203,.T.);
#3493=FACE_OUTER_BOUND('',#5204,.T.);
#3494=FACE_OUTER_BOUND('',#5205,.T.);
#3495=FACE_OUTER_BOUND('',#5206,.T.);
#3496=FACE_OUTER_BOUND('',#5207,.T.);
#3497=FACE_OUTER_BOUND('',#5208,.T.);
#3498=FACE_OUTER_BOUND('',#5209,.T.);
#3499=FACE_OUTER_BOUND('',#5211,.T.);
#3500=FACE_OUTER_BOUND('',#5213,.T.);
#3501=FACE_OUTER_BOUND('',#5214,.T.);
#3502=FACE_OUTER_BOUND('',#5215,.T.);
#3503=FACE_OUTER_BOUND('',#5216,.T.);
#3504=FACE_OUTER_BOUND('',#5217,.T.);
#3505=FACE_OUTER_BOUND('',#5218,.T.);
#5183=EDGE_LOOP('',(#22502,#22503,#22504,#22505,#22506));
#5184=EDGE_LOOP('',(#22507,#22508,#22509,#22510,#22511,#22512,#22513,#22514,
#22515));
#5185=EDGE_LOOP('',(#22516,#22517,#22518,#22519,#22520));
#5186=EDGE_LOOP('',(#22521,#22522,#22523,#22524));
#5187=EDGE_LOOP('',(#22525,#22526,#22527,#22528));
#5188=EDGE_LOOP('',(#22529));
#5189=EDGE_LOOP('',(#22530,#22531,#22532,#22533,#22534,#22535));
#5190=EDGE_LOOP('',(#22536));
#5191=EDGE_LOOP('',(#22537));
#5192=EDGE_LOOP('',(#22538));
#5193=EDGE_LOOP('',(#22539));
#5194=EDGE_LOOP('',(#22540));
#5195=EDGE_LOOP('',(#22541,#22542,#22543,#22544,#22545));
#5196=EDGE_LOOP('',(#22546,#22547,#22548,#22549,#22550));
#5197=EDGE_LOOP('',(#22551,#22552,#22553,#22554,#22555));
#5198=EDGE_LOOP('',(#22556,#22557,#22558,#22559,#22560));
#5199=EDGE_LOOP('',(#22561,#22562,#22563,#22564,#22565));
#5200=EDGE_LOOP('',(#22566,#22567,#22568,#22569,#22570));
#5201=EDGE_LOOP('',(#22571,#22572,#22573));
#5202=EDGE_LOOP('',(#22574,#22575,#22576,#22577));
#5203=EDGE_LOOP('',(#22578,#22579,#22580));
#5204=EDGE_LOOP('',(#22581,#22582,#22583));
#5205=EDGE_LOOP('',(#22584,#22585,#22586));
#5206=EDGE_LOOP('',(#22587,#22588,#22589));
#5207=EDGE_LOOP('',(#22590,#22591,#22592,#22593));
#5208=EDGE_LOOP('',(#22594,#22595,#22596,#22597));
#5209=EDGE_LOOP('',(#22598));
#5210=EDGE_LOOP('',(#22599));
#5211=EDGE_LOOP('',(#22600));
#5212=EDGE_LOOP('',(#22601));
#5213=EDGE_LOOP('',(#22602,#22603,#22604,#22605));
#5214=EDGE_LOOP('',(#22606,#22607,#22608,#22609));
#5215=EDGE_LOOP('',(#22610,#22611,#22612,#22613));
#5216=EDGE_LOOP('',(#22614,#22615,#22616,#22617));
#5217=EDGE_LOOP('',(#22618,#22619,#22620,#22621));
#5218=EDGE_LOOP('',(#22622,#22623,#22624,#22625));
#7135=LINE('',#56686,#9102);
#7136=LINE('',#56691,#9103);
#7137=LINE('',#56707,#9104);
#7138=LINE('',#56713,#9105);
#7139=LINE('',#56719,#9106);
#7140=LINE('',#56724,#9107);
#7141=LINE('',#56726,#9108);
#7142=LINE('',#56728,#9109);
#7143=LINE('',#56730,#9110);
#7144=LINE('',#56732,#9111);
#7145=LINE('',#56733,#9112);
#7146=LINE('',#56739,#9113);
#7147=LINE('',#56740,#9114);
#7148=LINE('',#56742,#9115);
#7149=LINE('',#56743,#9116);
#7150=LINE('',#56746,#9117);
#7151=LINE('',#56747,#9118);
#7152=LINE('',#56748,#9119);
#7153=LINE('',#56751,#9120);
#7154=LINE('',#56752,#9121);
#7155=LINE('',#56753,#9122);
#7156=LINE('',#56756,#9123);
#7157=LINE('',#56757,#9124);
#7158=LINE('',#56758,#9125);
#7159=LINE('',#56761,#9126);
#7160=LINE('',#56762,#9127);
#7161=LINE('',#56763,#9128);
#7162=LINE('',#56765,#9129);
#7163=LINE('',#56766,#9130);
#7164=LINE('',#56777,#9131);
#7165=LINE('',#56783,#9132);
#7166=LINE('',#56792,#9133);
#7167=LINE('',#56795,#9134);
#7168=LINE('',#56801,#9135);
#7169=LINE('',#56804,#9136);
#7170=LINE('',#56806,#9137);
#7171=LINE('',#56807,#9138);
#7172=LINE('',#56809,#9139);
#7173=LINE('',#56810,#9140);
#9102=VECTOR('',#34233,5.7);
#9103=VECTOR('',#34238,1664.2794823505);
#9104=VECTOR('',#34255,6.5);
#9105=VECTOR('',#34262,3.3225);
#9106=VECTOR('',#34269,4.);
#9107=VECTOR('',#34274,1000.);
#9108=VECTOR('',#34275,1000.);
#9109=VECTOR('',#34276,1000.);
#9110=VECTOR('',#34277,1000.);
#9111=VECTOR('',#34278,1000.);
#9112=VECTOR('',#34279,1000.);
#9113=VECTOR('',#34288,1000.);
#9114=VECTOR('',#34289,1000.);
#9115=VECTOR('',#34290,1000.);
#9116=VECTOR('',#34291,1000.);
#9117=VECTOR('',#34294,1000.);
#9118=VECTOR('',#34295,1000.);
#9119=VECTOR('',#34296,1000.);
#9120=VECTOR('',#34299,1000.);
#9121=VECTOR('',#34300,1000.);
#9122=VECTOR('',#34301,1000.);
#9123=VECTOR('',#34304,1000.);
#9124=VECTOR('',#34305,1000.);
#9125=VECTOR('',#34306,1000.);
#9126=VECTOR('',#34309,1000.);
#9127=VECTOR('',#34310,1000.);
#9128=VECTOR('',#34311,1000.);
#9129=VECTOR('',#34314,1000.);
#9130=VECTOR('',#34315,1000.);
#9131=VECTOR('',#34332,8.);
#9132=VECTOR('',#34339,4.);
#9133=VECTOR('',#34350,1000.);
#9134=VECTOR('',#34353,1000.);
#9135=VECTOR('',#34358,1000.);
#9136=VECTOR('',#34361,1000.);
#9137=VECTOR('',#34364,1000.);
#9138=VECTOR('',#34365,1000.);
#9139=VECTOR('',#34368,1000.);
#9140=VECTOR('',#34369,1000.);
#10242=CIRCLE('',#27317,6.5);
#10243=CIRCLE('',#27318,6.5);
#10244=CIRCLE('',#27319,5.7);
#10245=CIRCLE('',#27321,3.);
#10246=CIRCLE('',#27322,3.);
#10247=CIRCLE('',#27323,3.);
#10248=CIRCLE('',#27324,3.);
#10249=CIRCLE('',#27325,3.);
#10250=CIRCLE('',#27326,3.);
#10251=CIRCLE('',#27327,3.);
#10252=CIRCLE('',#27329,6.5);
#10253=CIRCLE('',#27331,3.3225);
#10254=CIRCLE('',#27332,3.3225);
#10255=CIRCLE('',#27334,4.);
#10256=CIRCLE('',#27335,4.);
#10257=CIRCLE('',#27353,8.);
#10258=CIRCLE('',#27354,8.);
#10259=CIRCLE('',#27356,4.);
#10260=CIRCLE('',#27357,4.);
#10261=CIRCLE('',#27361,7.25);
#10262=CIRCLE('',#27362,7.25);
#10263=CIRCLE('',#27364,4.);
#10264=CIRCLE('',#27365,4.);
#12425=VERTEX_POINT('',#56681);
#12426=VERTEX_POINT('',#56682);
#12427=VERTEX_POINT('',#56685);
#12428=VERTEX_POINT('',#56689);
#12429=VERTEX_POINT('',#56690);
#12430=VERTEX_POINT('',#56692);
#12431=VERTEX_POINT('',#56694);
#12432=VERTEX_POINT('',#56696);
#12433=VERTEX_POINT('',#56698);
#12434=VERTEX_POINT('',#56700);
#12435=VERTEX_POINT('',#56702);
#12436=VERTEX_POINT('',#56706);
#12437=VERTEX_POINT('',#56710);
#12438=VERTEX_POINT('',#56712);
#12439=VERTEX_POINT('',#56716);
#12440=VERTEX_POINT('',#56718);
#12441=VERTEX_POINT('',#56722);
#12442=VERTEX_POINT('',#56723);
#12443=VERTEX_POINT('',#56725);
#12444=VERTEX_POINT('',#56727);
#12445=VERTEX_POINT('',#56729);
#12446=VERTEX_POINT('',#56731);
#12447=VERTEX_POINT('',#56738);
#12448=VERTEX_POINT('',#56741);
#12449=VERTEX_POINT('',#56745);
#12450=VERTEX_POINT('',#56750);
#12451=VERTEX_POINT('',#56755);
#12452=VERTEX_POINT('',#56760);
#12453=VERTEX_POINT('',#56774);
#12454=VERTEX_POINT('',#56776);
#12455=VERTEX_POINT('',#56780);
#12456=VERTEX_POINT('',#56782);
#12457=VERTEX_POINT('',#56788);
#12458=VERTEX_POINT('',#56789);
#12459=VERTEX_POINT('',#56791);
#12460=VERTEX_POINT('',#56793);
#12461=VERTEX_POINT('',#56797);
#12462=VERTEX_POINT('',#56798);
#12463=VERTEX_POINT('',#56800);
#12464=VERTEX_POINT('',#56802);
#15796=EDGE_CURVE('',#12425,#12426,#10242,.T.);
#15797=EDGE_CURVE('',#12426,#12425,#10243,.T.);
#15798=EDGE_CURVE('',#12426,#12427,#7135,.T.);
#15799=EDGE_CURVE('',#12427,#12427,#10244,.T.);
#15800=EDGE_CURVE('',#12428,#12429,#7136,.T.);
#15801=EDGE_CURVE('',#12429,#12430,#10245,.T.);
#15802=EDGE_CURVE('',#12430,#12431,#10246,.T.);
#15803=EDGE_CURVE('',#12431,#12432,#10247,.T.);
#15804=EDGE_CURVE('',#12432,#12433,#10248,.T.);
#15805=EDGE_CURVE('',#12433,#12434,#10249,.T.);
#15806=EDGE_CURVE('',#12434,#12435,#10250,.T.);
#15807=EDGE_CURVE('',#12435,#12429,#10251,.T.);
#15808=EDGE_CURVE('',#12425,#12436,#7137,.T.);
#15809=EDGE_CURVE('',#12436,#12436,#10252,.T.);
#15810=EDGE_CURVE('',#12437,#12437,#10253,.T.);
#15811=EDGE_CURVE('',#12437,#12438,#7138,.T.);
#15812=EDGE_CURVE('',#12438,#12438,#10254,.T.);
#15813=EDGE_CURVE('',#12439,#12439,#10255,.T.);
#15814=EDGE_CURVE('',#12439,#12440,#7139,.T.);
#15815=EDGE_CURVE('',#12440,#12440,#10256,.T.);
#15816=EDGE_CURVE('',#12441,#12442,#7140,.T.);
#15817=EDGE_CURVE('',#12443,#12441,#7141,.T.);
#15818=EDGE_CURVE('',#12444,#12443,#7142,.T.);
#15819=EDGE_CURVE('',#12445,#12444,#7143,.T.);
#15820=EDGE_CURVE('',#12446,#12445,#7144,.T.);
#15821=EDGE_CURVE('',#12442,#12446,#7145,.T.);
#15822=EDGE_CURVE('',#12447,#12434,#7146,.T.);
#15823=EDGE_CURVE('',#12447,#12443,#7147,.T.);
#15824=EDGE_CURVE('',#12448,#12441,#7148,.T.);
#15825=EDGE_CURVE('',#12434,#12448,#7149,.T.);
#15826=EDGE_CURVE('',#12449,#12433,#7150,.T.);
#15827=EDGE_CURVE('',#12449,#12444,#7151,.T.);
#15828=EDGE_CURVE('',#12433,#12447,#7152,.T.);
#15829=EDGE_CURVE('',#12450,#12432,#7153,.T.);
#15830=EDGE_CURVE('',#12450,#12445,#7154,.T.);
#15831=EDGE_CURVE('',#12432,#12449,#7155,.T.);
#15832=EDGE_CURVE('',#12451,#12431,#7156,.T.);
#15833=EDGE_CURVE('',#12451,#12446,#7157,.T.);
#15834=EDGE_CURVE('',#12431,#12450,#7158,.T.);
#15835=EDGE_CURVE('',#12452,#12430,#7159,.T.);
#15836=EDGE_CURVE('',#12452,#12442,#7160,.T.);
#15837=EDGE_CURVE('',#12430,#12451,#7161,.T.);
#15838=EDGE_CURVE('',#12448,#12435,#7162,.T.);
#15839=EDGE_CURVE('',#12435,#12452,#7163,.T.);
#15840=EDGE_CURVE('',#12453,#12453,#10257,.T.);
#15841=EDGE_CURVE('',#12453,#12454,#7164,.T.);
#15842=EDGE_CURVE('',#12454,#12454,#10258,.T.);
#15843=EDGE_CURVE('',#12455,#12455,#10259,.T.);
#15844=EDGE_CURVE('',#12455,#12456,#7165,.T.);
#15845=EDGE_CURVE('',#12456,#12456,#10260,.T.);
#15846=EDGE_CURVE('',#12457,#12458,#10261,.T.);
#15847=EDGE_CURVE('',#12459,#12458,#7166,.T.);
#15848=EDGE_CURVE('',#12460,#12459,#10262,.T.);
#15849=EDGE_CURVE('',#12460,#12457,#7167,.T.);
#15850=EDGE_CURVE('',#12461,#12462,#10263,.T.);
#15851=EDGE_CURVE('',#12463,#12461,#7168,.T.);
#15852=EDGE_CURVE('',#12463,#12464,#10264,.T.);
#15853=EDGE_CURVE('',#12464,#12462,#7169,.T.);
#15854=EDGE_CURVE('',#12459,#12464,#7170,.T.);
#15855=EDGE_CURVE('',#12463,#12460,#7171,.T.);
#15856=EDGE_CURVE('',#12458,#12462,#7172,.T.);
#15857=EDGE_CURVE('',#12461,#12457,#7173,.T.);
#22502=ORIENTED_EDGE('',*,*,#15796,.F.);
#22503=ORIENTED_EDGE('',*,*,#15797,.F.);
#22504=ORIENTED_EDGE('',*,*,#15798,.T.);
#22505=ORIENTED_EDGE('',*,*,#15799,.F.);
#22506=ORIENTED_EDGE('',*,*,#15798,.F.);
#22507=ORIENTED_EDGE('',*,*,#15800,.T.);
#22508=ORIENTED_EDGE('',*,*,#15801,.T.);
#22509=ORIENTED_EDGE('',*,*,#15802,.T.);
#22510=ORIENTED_EDGE('',*,*,#15803,.T.);
#22511=ORIENTED_EDGE('',*,*,#15804,.T.);
#22512=ORIENTED_EDGE('',*,*,#15805,.T.);
#22513=ORIENTED_EDGE('',*,*,#15806,.T.);
#22514=ORIENTED_EDGE('',*,*,#15807,.T.);
#22515=ORIENTED_EDGE('',*,*,#15800,.F.);
#22516=ORIENTED_EDGE('',*,*,#15796,.T.);
#22517=ORIENTED_EDGE('',*,*,#15797,.T.);
#22518=ORIENTED_EDGE('',*,*,#15808,.T.);
#22519=ORIENTED_EDGE('',*,*,#15809,.T.);
#22520=ORIENTED_EDGE('',*,*,#15808,.F.);
#22521=ORIENTED_EDGE('',*,*,#15810,.F.);
#22522=ORIENTED_EDGE('',*,*,#15811,.T.);
#22523=ORIENTED_EDGE('',*,*,#15812,.T.);
#22524=ORIENTED_EDGE('',*,*,#15811,.F.);
#22525=ORIENTED_EDGE('',*,*,#15813,.F.);
#22526=ORIENTED_EDGE('',*,*,#15814,.T.);
#22527=ORIENTED_EDGE('',*,*,#15815,.T.);
#22528=ORIENTED_EDGE('',*,*,#15814,.F.);
#22529=ORIENTED_EDGE('',*,*,#15799,.T.);
#22530=ORIENTED_EDGE('',*,*,#15816,.F.);
#22531=ORIENTED_EDGE('',*,*,#15817,.F.);
#22532=ORIENTED_EDGE('',*,*,#15818,.F.);
#22533=ORIENTED_EDGE('',*,*,#15819,.F.);
#22534=ORIENTED_EDGE('',*,*,#15820,.F.);
#22535=ORIENTED_EDGE('',*,*,#15821,.F.);
#22536=ORIENTED_EDGE('',*,*,#15815,.F.);
#22537=ORIENTED_EDGE('',*,*,#15813,.T.);
#22538=ORIENTED_EDGE('',*,*,#15812,.F.);
#22539=ORIENTED_EDGE('',*,*,#15809,.F.);
#22540=ORIENTED_EDGE('',*,*,#15810,.T.);
#22541=ORIENTED_EDGE('',*,*,#15822,.F.);
#22542=ORIENTED_EDGE('',*,*,#15823,.T.);
#22543=ORIENTED_EDGE('',*,*,#15817,.T.);
#22544=ORIENTED_EDGE('',*,*,#15824,.F.);
#22545=ORIENTED_EDGE('',*,*,#15825,.F.);
#22546=ORIENTED_EDGE('',*,*,#15826,.F.);
#22547=ORIENTED_EDGE('',*,*,#15827,.T.);
#22548=ORIENTED_EDGE('',*,*,#15818,.T.);
#22549=ORIENTED_EDGE('',*,*,#15823,.F.);
#22550=ORIENTED_EDGE('',*,*,#15828,.F.);
#22551=ORIENTED_EDGE('',*,*,#15829,.F.);
#22552=ORIENTED_EDGE('',*,*,#15830,.T.);
#22553=ORIENTED_EDGE('',*,*,#15819,.T.);
#22554=ORIENTED_EDGE('',*,*,#15827,.F.);
#22555=ORIENTED_EDGE('',*,*,#15831,.F.);
#22556=ORIENTED_EDGE('',*,*,#15832,.F.);
#22557=ORIENTED_EDGE('',*,*,#15833,.T.);
#22558=ORIENTED_EDGE('',*,*,#15820,.T.);
#22559=ORIENTED_EDGE('',*,*,#15830,.F.);
#22560=ORIENTED_EDGE('',*,*,#15834,.F.);
#22561=ORIENTED_EDGE('',*,*,#15835,.F.);
#22562=ORIENTED_EDGE('',*,*,#15836,.T.);
#22563=ORIENTED_EDGE('',*,*,#15821,.T.);
#22564=ORIENTED_EDGE('',*,*,#15833,.F.);
#22565=ORIENTED_EDGE('',*,*,#15837,.F.);
#22566=ORIENTED_EDGE('',*,*,#15838,.F.);
#22567=ORIENTED_EDGE('',*,*,#15824,.T.);
#22568=ORIENTED_EDGE('',*,*,#15816,.T.);
#22569=ORIENTED_EDGE('',*,*,#15836,.F.);
#22570=ORIENTED_EDGE('',*,*,#15839,.F.);
#22571=ORIENTED_EDGE('',*,*,#15825,.T.);
#22572=ORIENTED_EDGE('',*,*,#15838,.T.);
#22573=ORIENTED_EDGE('',*,*,#15806,.F.);
#22574=ORIENTED_EDGE('',*,*,#15839,.T.);
#22575=ORIENTED_EDGE('',*,*,#15835,.T.);
#22576=ORIENTED_EDGE('',*,*,#15801,.F.);
#22577=ORIENTED_EDGE('',*,*,#15807,.F.);
#22578=ORIENTED_EDGE('',*,*,#15837,.T.);
#22579=ORIENTED_EDGE('',*,*,#15832,.T.);
#22580=ORIENTED_EDGE('',*,*,#15802,.F.);
#22581=ORIENTED_EDGE('',*,*,#15834,.T.);
#22582=ORIENTED_EDGE('',*,*,#15829,.T.);
#22583=ORIENTED_EDGE('',*,*,#15803,.F.);
#22584=ORIENTED_EDGE('',*,*,#15831,.T.);
#22585=ORIENTED_EDGE('',*,*,#15826,.T.);
#22586=ORIENTED_EDGE('',*,*,#15804,.F.);
#22587=ORIENTED_EDGE('',*,*,#15828,.T.);
#22588=ORIENTED_EDGE('',*,*,#15822,.T.);
#22589=ORIENTED_EDGE('',*,*,#15805,.F.);
#22590=ORIENTED_EDGE('',*,*,#15840,.F.);
#22591=ORIENTED_EDGE('',*,*,#15841,.T.);
#22592=ORIENTED_EDGE('',*,*,#15842,.T.);
#22593=ORIENTED_EDGE('',*,*,#15841,.F.);
#22594=ORIENTED_EDGE('',*,*,#15843,.F.);
#22595=ORIENTED_EDGE('',*,*,#15844,.T.);
#22596=ORIENTED_EDGE('',*,*,#15845,.T.);
#22597=ORIENTED_EDGE('',*,*,#15844,.F.);
#22598=ORIENTED_EDGE('',*,*,#15840,.T.);
#22599=ORIENTED_EDGE('',*,*,#15845,.F.);
#22600=ORIENTED_EDGE('',*,*,#15842,.F.);
#22601=ORIENTED_EDGE('',*,*,#15843,.T.);
#22602=ORIENTED_EDGE('',*,*,#15846,.T.);
#22603=ORIENTED_EDGE('',*,*,#15847,.F.);
#22604=ORIENTED_EDGE('',*,*,#15848,.F.);
#22605=ORIENTED_EDGE('',*,*,#15849,.T.);
#22606=ORIENTED_EDGE('',*,*,#15850,.F.);
#22607=ORIENTED_EDGE('',*,*,#15851,.F.);
#22608=ORIENTED_EDGE('',*,*,#15852,.T.);
#22609=ORIENTED_EDGE('',*,*,#15853,.T.);
#22610=ORIENTED_EDGE('',*,*,#15848,.T.);
#22611=ORIENTED_EDGE('',*,*,#15854,.T.);
#22612=ORIENTED_EDGE('',*,*,#15852,.F.);
#22613=ORIENTED_EDGE('',*,*,#15855,.T.);
#22614=ORIENTED_EDGE('',*,*,#15850,.T.);
#22615=ORIENTED_EDGE('',*,*,#15856,.F.);
#22616=ORIENTED_EDGE('',*,*,#15846,.F.);
#22617=ORIENTED_EDGE('',*,*,#15857,.F.);
#22618=ORIENTED_EDGE('',*,*,#15857,.T.);
#22619=ORIENTED_EDGE('',*,*,#15849,.F.);
#22620=ORIENTED_EDGE('',*,*,#15855,.F.);
#22621=ORIENTED_EDGE('',*,*,#15851,.T.);
#22622=ORIENTED_EDGE('',*,*,#15856,.T.);
#22623=ORIENTED_EDGE('',*,*,#15853,.F.);
#22624=ORIENTED_EDGE('',*,*,#15854,.F.);
#22625=ORIENTED_EDGE('',*,*,#15847,.T.);
#23140=CYLINDRICAL_SURFACE('',#27328,6.5);
#23141=CYLINDRICAL_SURFACE('',#27330,3.3225);
#23142=CYLINDRICAL_SURFACE('',#27333,4.);
#23143=CYLINDRICAL_SURFACE('',#27352,8.);
#23144=CYLINDRICAL_SURFACE('',#27355,4.);
#23145=CYLINDRICAL_SURFACE('',#27360,7.25);
#23146=CYLINDRICAL_SURFACE('',#27363,4.);
#24467=ADVANCED_FACE('',(#3475),#2153,.T.);
#24468=ADVANCED_FACE('',(#3476),#2154,.F.);
#24469=ADVANCED_FACE('',(#3477),#23140,.T.);
#24470=ADVANCED_FACE('',(#3478),#23141,.T.);
#24471=ADVANCED_FACE('',(#3479),#23142,.T.);
#24472=ADVANCED_FACE('',(#3480,#1333),#2063,.F.);
#24473=ADVANCED_FACE('',(#3481),#2064,.F.);
#24474=ADVANCED_FACE('',(#3482,#1334),#2065,.F.);
#24475=ADVANCED_FACE('',(#3483,#1335),#2066,.F.);
#24476=ADVANCED_FACE('',(#3484),#2067,.F.);
#24477=ADVANCED_FACE('',(#3485),#2068,.F.);
#24478=ADVANCED_FACE('',(#3486),#2069,.F.);
#24479=ADVANCED_FACE('',(#3487),#2070,.F.);
#24480=ADVANCED_FACE('',(#3488),#2071,.F.);
#24481=ADVANCED_FACE('',(#3489),#2072,.F.);
#24482=ADVANCED_FACE('',(#3490),#2073,.T.);
#24483=ADVANCED_FACE('',(#3491),#2074,.T.);
#24484=ADVANCED_FACE('',(#3492),#2075,.T.);
#24485=ADVANCED_FACE('',(#3493),#2076,.T.);
#24486=ADVANCED_FACE('',(#3494),#2077,.T.);
#24487=ADVANCED_FACE('',(#3495),#2078,.T.);
#24488=ADVANCED_FACE('',(#3496),#23143,.T.);
#24489=ADVANCED_FACE('',(#3497),#23144,.F.);
#24490=ADVANCED_FACE('',(#3498,#1336),#2079,.F.);
#24491=ADVANCED_FACE('',(#3499,#1337),#2080,.F.);
#24492=ADVANCED_FACE('',(#3500),#23145,.T.);
#24493=ADVANCED_FACE('',(#3501),#23146,.F.);
#24494=ADVANCED_FACE('',(#3502),#2081,.F.);
#24495=ADVANCED_FACE('',(#3503),#2082,.F.);
#24496=ADVANCED_FACE('',(#3504),#2083,.F.);
#24497=ADVANCED_FACE('',(#3505),#2084,.F.);
#24558=CLOSED_SHELL('',(#24467,#24468,#24469,#24470,#24471,#24472,#24473,
#24474,#24475,#24476,#24477,#24478,#24479,#24480,#24481,#24482,#24483,#24484,
#24485,#24486,#24487));
#24559=CLOSED_SHELL('',(#24488,#24489,#24490,#24491));
#24560=CLOSED_SHELL('',(#24492,#24493,#24494,#24495,#24496,#24497));
#27315=AXIS2_PLACEMENT_3D('',#56679,#34225,#34226);
#27316=AXIS2_PLACEMENT_3D('',#56680,#34227,#34228);
#27317=AXIS2_PLACEMENT_3D('',#56683,#34229,#34230);
#27318=AXIS2_PLACEMENT_3D('',#56684,#34231,#34232);
#27319=AXIS2_PLACEMENT_3D('',#56687,#34234,#34235);
#27320=AXIS2_PLACEMENT_3D('',#56688,#34236,#34237);
#27321=AXIS2_PLACEMENT_3D('',#56693,#34239,#34240);
#27322=AXIS2_PLACEMENT_3D('',#56695,#34241,#34242);
#27323=AXIS2_PLACEMENT_3D('',#56697,#34243,#34244);
#27324=AXIS2_PLACEMENT_3D('',#56699,#34245,#34246);
#27325=AXIS2_PLACEMENT_3D('',#56701,#34247,#34248);
#27326=AXIS2_PLACEMENT_3D('',#56703,#34249,#34250);
#27327=AXIS2_PLACEMENT_3D('',#56704,#34251,#34252);
#27328=AXIS2_PLACEMENT_3D('',#56705,#34253,#34254);
#27329=AXIS2_PLACEMENT_3D('',#56708,#34256,#34257);
#27330=AXIS2_PLACEMENT_3D('',#56709,#34258,#34259);
#27331=AXIS2_PLACEMENT_3D('',#56711,#34260,#34261);
#27332=AXIS2_PLACEMENT_3D('',#56714,#34263,#34264);
#27333=AXIS2_PLACEMENT_3D('',#56715,#34265,#34266);
#27334=AXIS2_PLACEMENT_3D('',#56717,#34267,#34268);
#27335=AXIS2_PLACEMENT_3D('',#56720,#34270,#34271);
#27336=AXIS2_PLACEMENT_3D('',#56721,#34272,#34273);
#27337=AXIS2_PLACEMENT_3D('',#56734,#34280,#34281);
#27338=AXIS2_PLACEMENT_3D('',#56735,#34282,#34283);
#27339=AXIS2_PLACEMENT_3D('',#56736,#34284,#34285);
#27340=AXIS2_PLACEMENT_3D('',#56737,#34286,#34287);
#27341=AXIS2_PLACEMENT_3D('',#56744,#34292,#34293);
#27342=AXIS2_PLACEMENT_3D('',#56749,#34297,#34298);
#27343=AXIS2_PLACEMENT_3D('',#56754,#34302,#34303);
#27344=AXIS2_PLACEMENT_3D('',#56759,#34307,#34308);
#27345=AXIS2_PLACEMENT_3D('',#56764,#34312,#34313);
#27346=AXIS2_PLACEMENT_3D('',#56767,#34316,#34317);
#27347=AXIS2_PLACEMENT_3D('',#56768,#34318,#34319);
#27348=AXIS2_PLACEMENT_3D('',#56769,#34320,#34321);
#27349=AXIS2_PLACEMENT_3D('',#56770,#34322,#34323);
#27350=AXIS2_PLACEMENT_3D('',#56771,#34324,#34325);
#27351=AXIS2_PLACEMENT_3D('',#56772,#34326,#34327);
#27352=AXIS2_PLACEMENT_3D('',#56773,#34328,#34329);
#27353=AXIS2_PLACEMENT_3D('',#56775,#34330,#34331);
#27354=AXIS2_PLACEMENT_3D('',#56778,#34333,#34334);
#27355=AXIS2_PLACEMENT_3D('',#56779,#34335,#34336);
#27356=AXIS2_PLACEMENT_3D('',#56781,#34337,#34338);
#27357=AXIS2_PLACEMENT_3D('',#56784,#34340,#34341);
#27358=AXIS2_PLACEMENT_3D('',#56785,#34342,#34343);
#27359=AXIS2_PLACEMENT_3D('',#56786,#34344,#34345);
#27360=AXIS2_PLACEMENT_3D('',#56787,#34346,#34347);
#27361=AXIS2_PLACEMENT_3D('',#56790,#34348,#34349);
#27362=AXIS2_PLACEMENT_3D('',#56794,#34351,#34352);
#27363=AXIS2_PLACEMENT_3D('',#56796,#34354,#34355);
#27364=AXIS2_PLACEMENT_3D('',#56799,#34356,#34357);
#27365=AXIS2_PLACEMENT_3D('',#56803,#34359,#34360);
#27366=AXIS2_PLACEMENT_3D('',#56805,#34362,#34363);
#27367=AXIS2_PLACEMENT_3D('',#56808,#34366,#34367);
#27368=AXIS2_PLACEMENT_3D('',#56811,#34370,#34371);
#27369=AXIS2_PLACEMENT_3D('',#56812,#34372,#34373);
#34225=DIRECTION('axis',(0.,0.,1.));
#34226=DIRECTION('refdir',(1.,0.,0.));
#34227=DIRECTION('center_axis',(1.,0.,0.));
#34228=DIRECTION('ref_axis',(0.,0.,-1.));
#34229=DIRECTION('center_axis',(1.,0.,0.));
#34230=DIRECTION('ref_axis',(0.,0.,-1.));
#34231=DIRECTION('center_axis',(1.,0.,0.));
#34232=DIRECTION('ref_axis',(0.,0.,-1.));
#34233=DIRECTION('',(-0.707106781186551,8.65956056235489E-17,-0.707106781186544));
#34234=DIRECTION('center_axis',(-1.,0.,0.));
#34235=DIRECTION('ref_axis',(0.,0.,-1.));
#34236=DIRECTION('center_axis',(-1.,7.08538566198487E-17,0.));
#34237=DIRECTION('ref_axis',(-7.08538566198487E-17,-1.,0.));
#34238=DIRECTION('',(-0.515038074910058,0.85716730070211,-1.04972719113862E-16));
#34239=DIRECTION('center_axis',(-1.,7.08538566198487E-17,0.));
#34240=DIRECTION('ref_axis',(-7.08538566198487E-17,-1.,0.));
#34241=DIRECTION('center_axis',(-1.,7.08538566198487E-17,0.));
#34242=DIRECTION('ref_axis',(-7.08538566198487E-17,-1.,0.));
#34243=DIRECTION('center_axis',(-1.,7.08538566198487E-17,0.));
#34244=DIRECTION('ref_axis',(-7.08538566198487E-17,-1.,0.));
#34245=DIRECTION('center_axis',(-1.,7.08538566198487E-17,0.));
#34246=DIRECTION('ref_axis',(-7.08538566198487E-17,-1.,0.));
#34247=DIRECTION('center_axis',(-1.,7.08538566198487E-17,0.));
#34248=DIRECTION('ref_axis',(-7.08538566198487E-17,-1.,0.));
#34249=DIRECTION('center_axis',(-1.,7.08538566198487E-17,0.));
#34250=DIRECTION('ref_axis',(-7.08538566198487E-17,-1.,0.));
#34251=DIRECTION('center_axis',(-1.,7.08538566198487E-17,0.));
#34252=DIRECTION('ref_axis',(-7.08538566198487E-17,-1.,0.));
#34253=DIRECTION('center_axis',(-1.,0.,0.));
#34254=DIRECTION('ref_axis',(0.,0.,1.));
#34255=DIRECTION('',(1.,0.,0.));
#34256=DIRECTION('center_axis',(-1.,0.,0.));
#34257=DIRECTION('ref_axis',(0.,0.,1.));
#34258=DIRECTION('center_axis',(-1.,0.,0.));
#34259=DIRECTION('ref_axis',(0.,0.,1.));
#34260=DIRECTION('center_axis',(-1.,0.,0.));
#34261=DIRECTION('ref_axis',(0.,0.,1.));
#34262=DIRECTION('',(1.,0.,0.));
#34263=DIRECTION('center_axis',(-1.,0.,0.));
#34264=DIRECTION('ref_axis',(0.,0.,1.));
#34265=DIRECTION('center_axis',(-1.,0.,0.));
#34266=DIRECTION('ref_axis',(0.,0.,1.));
#34267=DIRECTION('center_axis',(-1.,0.,0.));
#34268=DIRECTION('ref_axis',(0.,0.,1.));
#34269=DIRECTION('',(1.,0.,0.));
#34270=DIRECTION('center_axis',(-1.,0.,0.));
#34271=DIRECTION('ref_axis',(0.,0.,1.));
#34272=DIRECTION('center_axis',(1.,0.,0.));
#34273=DIRECTION('ref_axis',(0.,0.,-1.));
#34274=DIRECTION('',(0.,0.5,-0.866025403784439));
#34275=DIRECTION('',(0.,1.,-1.25192883228097E-16));
#34276=DIRECTION('',(0.,0.5,0.866025403784439));
#34277=DIRECTION('',(0.,-0.5,0.866025403784439));
#34278=DIRECTION('',(0.,-1.,0.));
#34279=DIRECTION('',(0.,-0.5,-0.866025403784439));
#34280=DIRECTION('center_axis',(-1.,0.,0.));
#34281=DIRECTION('ref_axis',(0.,0.,1.));
#34282=DIRECTION('center_axis',(1.,0.,0.));
#34283=DIRECTION('ref_axis',(0.,0.,-1.));
#34284=DIRECTION('center_axis',(-1.,0.,0.));
#34285=DIRECTION('ref_axis',(0.,0.,1.));
#34286=DIRECTION('center_axis',(0.,1.25192883228097E-16,1.));
#34287=DIRECTION('ref_axis',(0.,-1.,1.25192883228097E-16));
#34288=DIRECTION('',(0.,1.,-1.25192883228097E-16));
#34289=DIRECTION('',(-1.,0.,0.));
#34290=DIRECTION('',(-1.,0.,0.));
#34291=DIRECTION('',(0.,1.,-1.25192883228097E-16));
#34292=DIRECTION('center_axis',(0.,-0.866025403784439,0.5));
#34293=DIRECTION('ref_axis',(0.,-0.5,-0.866025403784439));
#34294=DIRECTION('',(0.,0.5,0.866025403784439));
#34295=DIRECTION('',(-1.,0.,0.));
#34296=DIRECTION('',(0.,0.5,0.866025403784439));
#34297=DIRECTION('center_axis',(0.,-0.866025403784439,-0.5));
#34298=DIRECTION('ref_axis',(0.,0.5,-0.866025403784439));
#34299=DIRECTION('',(0.,-0.5,0.866025403784439));
#34300=DIRECTION('',(-1.,0.,0.));
#34301=DIRECTION('',(0.,-0.5,0.866025403784439));
#34302=DIRECTION('center_axis',(0.,0.,-1.));
#34303=DIRECTION('ref_axis',(-1.,0.,0.));
#34304=DIRECTION('',(0.,-1.,0.));
#34305=DIRECTION('',(-1.,0.,0.));
#34306=DIRECTION('',(0.,-1.,0.));
#34307=DIRECTION('center_axis',(0.,0.866025403784439,-0.5));
#34308=DIRECTION('ref_axis',(0.,0.5,0.866025403784439));
#34309=DIRECTION('',(0.,-0.5,-0.866025403784439));
#34310=DIRECTION('',(-1.,0.,0.));
#34311=DIRECTION('',(0.,-0.5,-0.866025403784439));
#34312=DIRECTION('center_axis',(0.,0.866025403784439,0.5));
#34313=DIRECTION('ref_axis',(0.,-0.5,0.866025403784439));
#34314=DIRECTION('',(0.,0.5,-0.866025403784439));
#34315=DIRECTION('',(0.,0.5,-0.866025403784439));
#34316=DIRECTION('center_axis',(-1.,0.,0.));
#34317=DIRECTION('ref_axis',(0.,0.,1.));
#34318=DIRECTION('center_axis',(-1.,0.,0.));
#34319=DIRECTION('ref_axis',(0.,0.,1.));
#34320=DIRECTION('center_axis',(-1.,0.,0.));
#34321=DIRECTION('ref_axis',(0.,0.,1.));
#34322=DIRECTION('center_axis',(-1.,0.,0.));
#34323=DIRECTION('ref_axis',(0.,0.,1.));
#34324=DIRECTION('center_axis',(-1.,0.,0.));
#34325=DIRECTION('ref_axis',(0.,0.,1.));
#34326=DIRECTION('center_axis',(-1.,0.,0.));
#34327=DIRECTION('ref_axis',(0.,0.,1.));
#34328=DIRECTION('center_axis',(-1.,-1.17680295328379E-17,0.));
#34329=DIRECTION('ref_axis',(1.17680295328379E-17,-1.,0.));
#34330=DIRECTION('center_axis',(-1.,-1.17680295328379E-17,0.));
#34331=DIRECTION('ref_axis',(1.17680295328379E-17,-1.,0.));
#34332=DIRECTION('',(1.,1.17680295328379E-17,0.));
#34333=DIRECTION('center_axis',(-1.,-1.17680295328379E-17,0.));
#34334=DIRECTION('ref_axis',(1.17680295328379E-17,-1.,0.));
#34335=DIRECTION('center_axis',(-1.,-1.17680295328379E-17,0.));
#34336=DIRECTION('ref_axis',(1.17680295328379E-17,-1.,0.));
#34337=DIRECTION('center_axis',(-1.,-1.17680295328379E-17,0.));
#34338=DIRECTION('ref_axis',(1.17680295328379E-17,-1.,0.));
#34339=DIRECTION('',(-1.,-1.17680295328379E-17,0.));
#34340=DIRECTION('center_axis',(-1.,-1.17680295328379E-17,0.));
#34341=DIRECTION('ref_axis',(1.17680295328379E-17,-1.,0.));
#34342=DIRECTION('center_axis',(1.,1.17680295328379E-17,0.));
#34343=DIRECTION('ref_axis',(-1.17680295328379E-17,1.,0.));
#34344=DIRECTION('center_axis',(-1.,-1.17680295328379E-17,0.));
#34345=DIRECTION('ref_axis',(1.17680295328379E-17,-1.,0.));
#34346=DIRECTION('center_axis',(-1.,-3.79192062724778E-17,0.));
#34347=DIRECTION('ref_axis',(-8.5006563062609E-33,1.83697019872103E-16,
-1.));
#34348=DIRECTION('center_axis',(-1.,-3.79192062724778E-17,0.));
#34349=DIRECTION('ref_axis',(3.79192062724778E-17,-1.,0.));
#34350=DIRECTION('',(1.,0.,0.));
#34351=DIRECTION('center_axis',(-1.,-3.79192062724778E-17,0.));
#34352=DIRECTION('ref_axis',(3.79192062724778E-17,-1.,0.));
#34353=DIRECTION('',(1.,0.,0.));
#34354=DIRECTION('center_axis',(-1.,-3.79192062724778E-17,0.));
#34355=DIRECTION('ref_axis',(-7.70371977754894E-33,1.83697019872103E-16,
-1.));
#34356=DIRECTION('center_axis',(-1.,-3.79192062724778E-17,0.));
#34357=DIRECTION('ref_axis',(3.79192062724778E-17,-1.,0.));
#34358=DIRECTION('',(1.,0.,0.));
#34359=DIRECTION('center_axis',(-1.,-3.79192062724778E-17,0.));
#34360=DIRECTION('ref_axis',(3.79192062724778E-17,-1.,0.));
#34361=DIRECTION('',(1.,0.,0.));
#34362=DIRECTION('center_axis',(1.,3.79192062724778E-17,0.));
#34363=DIRECTION('ref_axis',(-3.79192062724778E-17,1.,0.));
#34364=DIRECTION('',(0.,-6.27682405047592E-17,-1.));
#34365=DIRECTION('',(0.,-6.27682405047592E-17,1.));
#34366=DIRECTION('center_axis',(-1.,-3.79192062724778E-17,0.));
#34367=DIRECTION('ref_axis',(3.79192062724778E-17,-1.,0.));
#34368=DIRECTION('',(0.,-6.27682405047592E-17,-1.));
#34369=DIRECTION('',(0.,-6.27682405047592E-17,1.));
#34370=DIRECTION('center_axis',(0.,1.,6.27682405047592E-17));
#34371=DIRECTION('ref_axis',(0.,-6.27682405047592E-17,1.));
#34372=DIRECTION('center_axis',(0.,-1.,6.27682405047592E-17));
#34373=DIRECTION('ref_axis',(0.,-6.27682405047592E-17,-1.));
#56679=CARTESIAN_POINT('',(0.,0.,0.));
#56680=CARTESIAN_POINT('Origin',(-11.6,0.,0.));
#56681=CARTESIAN_POINT('',(-10.8,7.9602041944578E-16,-6.5));
#56682=CARTESIAN_POINT('',(-10.8,-7.9602041944578E-16,6.5));
#56683=CARTESIAN_POINT('Origin',(-10.8,0.,0.));
#56684=CARTESIAN_POINT('Origin',(-10.8,0.,0.));
#56685=CARTESIAN_POINT('',(-11.6,-6.98048675513991E-16,5.7));
#56686=CARTESIAN_POINT('',(-11.6,-6.98048675513991E-16,5.7));
#56687=CARTESIAN_POINT('Origin',(-11.6,0.,0.));
#56688=CARTESIAN_POINT('Origin',(-1005.79741814292,7.0442721316922E-14,
0.));
#56689=CARTESIAN_POINT('',(-5.7974181429173,-4.11135302926673E-16,0.));
#56690=CARTESIAN_POINT('',(-7.60000000000019,3.0000000000004,-3.67394039744256E-16));
#56691=CARTESIAN_POINT('',(-1005.79741814292,1664.2794823505,-2.03815454094715E-13));
#56692=CARTESIAN_POINT('',(-7.6,2.59807621135332,-1.5));
#56693=CARTESIAN_POINT('Origin',(-7.6,-2.83415426479395E-16,0.));
#56694=CARTESIAN_POINT('',(-7.6,-2.83415426479395E-16,-3.));
#56695=CARTESIAN_POINT('Origin',(-7.6,-2.83415426479395E-16,0.));
#56696=CARTESIAN_POINT('',(-7.6,-2.59807621135332,-1.5));
#56697=CARTESIAN_POINT('Origin',(-7.6,-2.83415426479395E-16,0.));
#56698=CARTESIAN_POINT('',(-7.6,-2.59807621135332,1.5));
#56699=CARTESIAN_POINT('Origin',(-7.6,-2.83415426479395E-16,0.));
#56700=CARTESIAN_POINT('',(-7.6,9.2163223204895E-17,3.));
#56701=CARTESIAN_POINT('Origin',(-7.6,-2.83415426479395E-16,0.));
#56702=CARTESIAN_POINT('',(-7.6,2.59807621135331,1.5));
#56703=CARTESIAN_POINT('Origin',(-7.6,-2.83415426479395E-16,0.));
#56704=CARTESIAN_POINT('Origin',(-7.6,-2.83415426479395E-16,0.));
#56705=CARTESIAN_POINT('Origin',(-11.6,0.,0.));
#56706=CARTESIAN_POINT('',(-3.6,-7.96020419445779E-16,-6.5));
#56707=CARTESIAN_POINT('',(-11.6,-7.96020419445779E-16,-6.5));
#56708=CARTESIAN_POINT('Origin',(-3.6,0.,0.));
#56709=CARTESIAN_POINT('Origin',(-11.6,0.,0.));
#56710=CARTESIAN_POINT('',(-3.6,-4.06888899016708E-16,-3.3225));
#56711=CARTESIAN_POINT('Origin',(-3.6,0.,0.));
#56712=CARTESIAN_POINT('',(4.8,-4.06888899016708E-16,-3.3225));
#56713=CARTESIAN_POINT('',(-11.6,-4.06888899016708E-16,-3.3225));
#56714=CARTESIAN_POINT('Origin',(4.8,0.,0.));
#56715=CARTESIAN_POINT('Origin',(-11.6,0.,0.));
#56716=CARTESIAN_POINT('',(4.8,-4.89858719658941E-16,-4.));
#56717=CARTESIAN_POINT('Origin',(4.8,0.,0.));
#56718=CARTESIAN_POINT('',(41.4,-4.89858719658941E-16,-4.));
#56719=CARTESIAN_POINT('',(-11.6,-4.89858719658941E-16,-4.));
#56720=CARTESIAN_POINT('Origin',(41.4,0.,0.));
#56721=CARTESIAN_POINT('Origin',(-11.6,0.,0.));
#56722=CARTESIAN_POINT('',(-11.6,1.73205080756888,3.));
#56723=CARTESIAN_POINT('',(-11.6,3.46410161513775,-1.37814221648228E-16));
#56724=CARTESIAN_POINT('',(-11.6,1.73205080756888,3.));
#56725=CARTESIAN_POINT('',(-11.6,-1.73205080756888,3.));
#56726=CARTESIAN_POINT('',(-11.6,-1.73205080756888,3.));
#56727=CARTESIAN_POINT('',(-11.6,-3.46410161513776,-2.41656538721699E-16));
#56728=CARTESIAN_POINT('',(-11.6,-3.46410161513776,-2.41656538721699E-16));
#56729=CARTESIAN_POINT('',(-11.6,-1.73205080756888,-3.));
#56730=CARTESIAN_POINT('',(-11.6,-1.73205080756888,-3.));
#56731=CARTESIAN_POINT('',(-11.6,1.73205080756888,-3.));
#56732=CARTESIAN_POINT('',(-11.6,1.73205080756888,-3.));
#56733=CARTESIAN_POINT('',(-11.6,3.46410161513775,-1.37814221648228E-16));
#56734=CARTESIAN_POINT('Origin',(41.4,4.,0.));
#56735=CARTESIAN_POINT('Origin',(4.8,4.,0.));
#56736=CARTESIAN_POINT('Origin',(-3.6,3.3225,0.));
#56737=CARTESIAN_POINT('Origin',(-7.6,-1.73205080756888,3.));
#56738=CARTESIAN_POINT('',(-7.6,-1.73205080756888,3.));
#56739=CARTESIAN_POINT('',(-7.6,-1.73205080756888,3.));
#56740=CARTESIAN_POINT('',(-7.6,-1.73205080756888,3.));
#56741=CARTESIAN_POINT('',(-7.6,1.73205080756888,3.));
#56742=CARTESIAN_POINT('',(-7.6,1.73205080756888,3.));
#56743=CARTESIAN_POINT('',(-7.6,-1.73205080756888,3.));
#56744=CARTESIAN_POINT('Origin',(-7.6,-3.46410161513776,-2.41656538721699E-16));
#56745=CARTESIAN_POINT('',(-7.6,-3.46410161513776,-2.41656538721699E-16));
#56746=CARTESIAN_POINT('',(-7.6,-3.46410161513776,-2.41656538721699E-16));
#56747=CARTESIAN_POINT('',(-7.6,-3.46410161513776,-2.41656538721699E-16));
#56748=CARTESIAN_POINT('',(-7.6,-3.46410161513776,-2.41656538721699E-16));
#56749=CARTESIAN_POINT('Origin',(-7.6,-1.73205080756888,-3.));
#56750=CARTESIAN_POINT('',(-7.6,-1.73205080756888,-3.));
#56751=CARTESIAN_POINT('',(-7.6,-1.73205080756888,-3.));
#56752=CARTESIAN_POINT('',(-7.6,-1.73205080756888,-3.));
#56753=CARTESIAN_POINT('',(-7.6,-1.73205080756888,-3.));
#56754=CARTESIAN_POINT('Origin',(-7.6,1.73205080756888,-3.));
#56755=CARTESIAN_POINT('',(-7.6,1.73205080756888,-3.));
#56756=CARTESIAN_POINT('',(-7.6,1.73205080756888,-3.));
#56757=CARTESIAN_POINT('',(-7.6,1.73205080756888,-3.));
#56758=CARTESIAN_POINT('',(-7.6,1.73205080756888,-3.));
#56759=CARTESIAN_POINT('Origin',(-7.6,3.46410161513775,-1.37814221648228E-16));
#56760=CARTESIAN_POINT('',(-7.6,3.46410161513775,-1.37814221648228E-16));
#56761=CARTESIAN_POINT('',(-7.6,3.46410161513775,-1.37814221648228E-16));
#56762=CARTESIAN_POINT('',(-7.6,3.46410161513775,-1.37814221648228E-16));
#56763=CARTESIAN_POINT('',(-7.6,3.46410161513775,-1.37814221648228E-16));
#56764=CARTESIAN_POINT('Origin',(-7.6,1.73205080756888,3.));
#56765=CARTESIAN_POINT('',(-7.6,1.73205080756888,3.));
#56766=CARTESIAN_POINT('',(-7.6,1.73205080756888,3.));
#56767=CARTESIAN_POINT('Origin',(-7.6,0.,0.));
#56768=CARTESIAN_POINT('Origin',(-7.6,0.,0.));
#56769=CARTESIAN_POINT('Origin',(-7.6,0.,0.));
#56770=CARTESIAN_POINT('Origin',(-7.6,0.,0.));
#56771=CARTESIAN_POINT('Origin',(-7.6,0.,0.));
#56772=CARTESIAN_POINT('Origin',(-7.6,0.,0.));
#56773=CARTESIAN_POINT('Origin',(-11.6,-1.3650914258092E-16,0.));
#56774=CARTESIAN_POINT('',(-1.6,8.,-9.79717439317883E-16));
#56775=CARTESIAN_POINT('Origin',(-1.6,-1.88288472525407E-17,0.));
#56776=CARTESIAN_POINT('',(0.,8.,-9.79717439317883E-16));
#56777=CARTESIAN_POINT('',(-11.6,8.,-9.79717439317883E-16));
#56778=CARTESIAN_POINT('Origin',(0.,0.,0.));
#56779=CARTESIAN_POINT('Origin',(-11.6,-1.3650914258092E-16,0.));
#56780=CARTESIAN_POINT('',(0.,4.,-4.89858719658941E-16));
#56781=CARTESIAN_POINT('Origin',(0.,0.,0.));
#56782=CARTESIAN_POINT('',(-1.6,4.,-4.89858719658941E-16));
#56783=CARTESIAN_POINT('',(-11.6,4.,-4.89858719658941E-16));
#56784=CARTESIAN_POINT('Origin',(-1.6,-1.88288472525407E-17,0.));
#56785=CARTESIAN_POINT('Origin',(-1.6,8.,0.));
#56786=CARTESIAN_POINT('Origin',(-3.29697758852514E-16,8.,0.));
#56787=CARTESIAN_POINT('Origin',(-3.6,-1.3650914258092E-16,0.));
#56788=CARTESIAN_POINT('',(-1.6,1.815,7.01913634288436));
#56789=CARTESIAN_POINT('',(-1.6,-1.815,7.01913634288436));
#56790=CARTESIAN_POINT('Origin',(-1.6,-6.06707300359645E-17,0.));
#56791=CARTESIAN_POINT('',(-3.6,-1.815,7.01913634288436));
#56792=CARTESIAN_POINT('',(-3.6,-1.815,7.01913634288436));
#56793=CARTESIAN_POINT('',(-3.6,1.815,7.01913634288436));
#56794=CARTESIAN_POINT('Origin',(-3.6,-1.3650914258092E-16,0.));
#56795=CARTESIAN_POINT('',(-3.6,1.815,7.01913634288436));
#56796=CARTESIAN_POINT('Origin',(-3.6,-1.3650914258092E-16,0.));
#56797=CARTESIAN_POINT('',(-1.6,1.815,3.56451609619034));
#56798=CARTESIAN_POINT('',(-1.6,-1.815,3.56451609619034));
#56799=CARTESIAN_POINT('Origin',(-1.6,-6.06707300359645E-17,0.));
#56800=CARTESIAN_POINT('',(-3.6,1.815,3.56451609619034));
#56801=CARTESIAN_POINT('',(-3.6,1.815,3.56451609619034));
#56802=CARTESIAN_POINT('',(-3.6,-1.815,3.56451609619034));
#56803=CARTESIAN_POINT('Origin',(-3.6,-1.3650914258092E-16,0.));
#56804=CARTESIAN_POINT('',(-3.6,-1.815,3.56451609619034));
#56805=CARTESIAN_POINT('Origin',(-3.6,7.25,0.));
#56806=CARTESIAN_POINT('',(-3.6,-1.815,7.01913634288436));
#56807=CARTESIAN_POINT('',(-3.6,1.815,7.01913634288436));
#56808=CARTESIAN_POINT('Origin',(-1.6,7.25,0.));
#56809=CARTESIAN_POINT('',(-1.6,-1.815,7.01913634288436));
#56810=CARTESIAN_POINT('',(-1.6,1.815,7.01913634288436));
#56811=CARTESIAN_POINT('Origin',(-3.6,1.815,7.01913634288436));
#56812=CARTESIAN_POINT('Origin',(-3.6,-1.815,7.01913634288436));
#57037=UNCERTAINTY_MEASURE_WITH_UNIT(LENGTH_MEASURE(0.01),#57080,
'DISTANCE_ACCURACY_VALUE',
'Maximum model space distance between geometric entities at asserted c
onnectivities');
#57040=UNCERTAINTY_MEASURE_WITH_UNIT(LENGTH_MEASURE(0.01),#57080,
'DISTANCE_ACCURACY_VALUE',
'Maximum model space distance between geometric entities at asserted c
onnectivities');
#57076=(
GEOMETRIC_REPRESENTATION_CONTEXT(3)
GLOBAL_UNCERTAINTY_ASSIGNED_CONTEXT((#57037))
GLOBAL_UNIT_ASSIGNED_CONTEXT((#57080,#57082,#57083))
REPRESENTATION_CONTEXT('','3D')
);
#57079=(
GEOMETRIC_REPRESENTATION_CONTEXT(3)
GLOBAL_UNCERTAINTY_ASSIGNED_CONTEXT((#57040))
GLOBAL_UNIT_ASSIGNED_CONTEXT((#57080,#57082,#57083))
REPRESENTATION_CONTEXT('','3D')
);
#57080=(
LENGTH_UNIT()
NAMED_UNIT(*)
SI_UNIT(.MILLI.,.METRE.)
);
#57082=(
NAMED_UNIT(*)
PLANE_ANGLE_UNIT()
SI_UNIT($,.RADIAN.)
);
#57083=(
NAMED_UNIT(*)
SI_UNIT($,.STERADIAN.)
SOLID_ANGLE_UNIT()
);
#57119=SHAPE_DEFINITION_REPRESENTATION(#57183,#57284);
#57183=PRODUCT_DEFINITION_SHAPE('',$,#57323);
#57284=SHAPE_REPRESENTATION('',(#27315),#57076);
#57287=PRODUCT_DEFINITION_CONTEXT('part definition',#57403,'design');
#57323=PRODUCT_DEFINITION('Low Head Cap Screw M8x45',
'Low Head Cap Screw M8x45',#57361,#57287);
#57361=PRODUCT_DEFINITION_FORMATION('',$,#57440);
#57403=APPLICATION_CONTEXT(
'Core Data for Automotive Mechanical Design Process');
#57404=PRODUCT_CONTEXT('part definition',#57403,'mechanical');
#57440=PRODUCT('Low Head Cap Screw M8x45','Low Head Cap Screw M8x45',$,
(#57404));
#57444=PRESENTATION_STYLE_ASSIGNMENT((#57446));
#57446=SURFACE_STYLE_USAGE(.BOTH.,#57448);
#57448=SURFACE_SIDE_STYLE('',(#57450));
#57450=SURFACE_STYLE_FILL_AREA(#57452);
#57452=FILL_AREA_STYLE('Opaque(202,209,238)',(#57454));
#57454=FILL_AREA_STYLE_COLOUR('Opaque(202,209,238)',#57456);
#57456=COLOUR_RGB('Opaque(202,209,238)',0.792156862745098,0.819607843137255,
0.933333333333333);
ENDSEC;
END-ISO-10303-21;
